ISO-10303-21;
HEADER;
/* Generated by software containing ST-Developer
 * from STEP Tools, Inc. (www.steptools.com) 
 */

FILE_DESCRIPTION(
/* description */ ('Manual piston pump'),
/* implementation_level */ '2;1');

FILE_NAME(
/* name */ 'M4x14 manifold screw.step',
/* time_stamp */ '2026-11-02T16:54:23-08:00',
/* author */ (''),
/* organization */ (''),
/* preprocessor_version */ 'ST-DEVELOPER v20.2',
/* originating_system */ 'Autodesk Translation Framework v15.17.0.0',
/* authorisation */ '');

FILE_SCHEMA (('AUTOMOTIVE_DESIGN { 1 0 10303 214 3 1 1 }'));
ENDSEC;

DATA;
#10=MECHANICAL_DESIGN_GEOMETRIC_PRESENTATION_REPRESENTATION('',(#734),#19043);
#524=ORIENTED_CLOSED_SHELL('',*,#9520,.F.);
#541=CONICAL_SURFACE('',#11044,0.325,0.785398163397448);
#542=CONICAL_SURFACE('',#11048,0.335,0.785398163397448);
#543=CONICAL_SURFACE('',#11052,0.21,0.463647609000806);
#555=BREP_WITH_VOIDS('Body1',#9521,(#524));
#600=SHAPE_REPRESENTATION_RELATIONSHIP('SRR','None',#19348,#663);
#663=ADVANCED_BREP_SHAPE_REPRESENTATION('',(#555),#19015);
#734=STYLED_ITEM('',(#19663),#555);
#997=FACE_BOUND('',#2437,.T.);
#1232=CYLINDRICAL_SURFACE('',#11046,0.35);
#1233=CYLINDRICAL_SURFACE('',#11054,0.1954);
#1678=FACE_OUTER_BOUND('',#2423,.T.);
#1679=FACE_OUTER_BOUND('',#2424,.T.);
#1680=FACE_OUTER_BOUND('',#2425,.T.);
#1681=FACE_OUTER_BOUND('',#2426,.T.);
#1682=FACE_OUTER_BOUND('',#2427,.T.);
#1683=FACE_OUTER_BOUND('',#2428,.T.);
#1684=FACE_OUTER_BOUND('',#2429,.T.);
#1685=FACE_OUTER_BOUND('',#2430,.T.);
#1686=FACE_OUTER_BOUND('',#2431,.T.);
#1687=FACE_OUTER_BOUND('',#2432,.T.);
#1688=FACE_OUTER_BOUND('',#2433,.T.);
#1689=FACE_OUTER_BOUND('',#2434,.T.);
#1690=FACE_OUTER_BOUND('',#2435,.T.);
#1691=FACE_OUTER_BOUND('',#2436,.T.);
#1692=FACE_OUTER_BOUND('',#2438,.T.);
#1693=FACE_OUTER_BOUND('',#2439,.T.);
#2423=EDGE_LOOP('',(#7859,#7860,#7861,#7862));
#2424=EDGE_LOOP('',(#7863,#7864,#7865,#7866));
#2425=EDGE_LOOP('',(#7867,#7868,#7869,#7870));
#2426=EDGE_LOOP('',(#7871,#7872,#7873,#7874));
#2427=EDGE_LOOP('',(#7875,#7876,#7877,#7878));
#2428=EDGE_LOOP('',(#7879,#7880,#7881,#7882));
#2429=EDGE_LOOP('',(#7883,#7884,#7885,#7886,#7887,#7888));
#2430=EDGE_LOOP('',(#7889,#7890,#7891,#7892,#7893,#7894));
#2431=EDGE_LOOP('',(#7895));
#2432=EDGE_LOOP('',(#7896));
#2433=EDGE_LOOP('',(#7897,#7898,#7899,#7900));
#2434=EDGE_LOOP('',(#7901,#7902,#7903,#7904));
#2435=EDGE_LOOP('',(#7905,#7906,#7907,#7908));
#2436=EDGE_LOOP('',(#7909));
#2437=EDGE_LOOP('',(#7910));
#2438=EDGE_LOOP('',(#7911,#7912,#7913,#7914));
#2439=EDGE_LOOP('',(#7915,#7916,#7917,#7918));
#3011=CIRCLE('',#11041,0.1954);
#3012=CIRCLE('',#11043,0.3);
#3013=CIRCLE('',#11045,0.35);
#3014=CIRCLE('',#11047,0.35);
#3015=CIRCLE('',#11049,0.32);
#3016=CIRCLE('',#11051,0.22);
#3017=CIRCLE('',#11053,0.1954);
#3546=LINE('',#17860,#4150);
#3547=LINE('',#17862,#4151);
#3548=LINE('',#17864,#4152);
#3549=LINE('',#17865,#4153);
#3550=LINE('',#17868,#4154);
#3551=LINE('',#17870,#4155);
#3552=LINE('',#17871,#4156);
#3553=LINE('',#17874,#4157);
#3554=LINE('',#17876,#4158);
#3555=LINE('',#17877,#4159);
#3556=LINE('',#17880,#4160);
#3557=LINE('',#17882,#4161);
#3558=LINE('',#17883,#4162);
#3559=LINE('',#17886,#4163);
#3560=LINE('',#17888,#4164);
#3561=LINE('',#17889,#4165);
#3562=LINE('',#17891,#4166);
#3563=LINE('',#17892,#4167);
#3564=LINE('',#17904,#4168);
#3565=LINE('',#17908,#4169);
#3566=LINE('',#17912,#4170);
#3567=LINE('',#17919,#4171);
#3568=LINE('',#17921,#4172);
#4150=VECTOR('',#13474,1.);
#4151=VECTOR('',#13475,1.);
#4152=VECTOR('',#13476,1.);
#4153=VECTOR('',#13477,1.);
#4154=VECTOR('',#13480,1.);
#4155=VECTOR('',#13481,1.);
#4156=VECTOR('',#13482,1.);
#4157=VECTOR('',#13485,1.);
#4158=VECTOR('',#13486,1.);
#4159=VECTOR('',#13487,1.);
#4160=VECTOR('',#13490,1.);
#4161=VECTOR('',#13491,1.);
#4162=VECTOR('',#13492,1.);
#4163=VECTOR('',#13495,1.);
#4164=VECTOR('',#13496,1.);
#4165=VECTOR('',#13497,1.);
#4166=VECTOR('',#13500,1.);
#4167=VECTOR('',#13501,1.);
#4168=VECTOR('',#13518,0.325);
#4169=VECTOR('',#13523,0.35);
#4170=VECTOR('',#13528,0.335);
#4171=VECTOR('',#13537,0.21);
#4172=VECTOR('',#13540,0.2);
#4890=VERTEX_POINT('',#17858);
#4891=VERTEX_POINT('',#17859);
#4892=VERTEX_POINT('',#17861);
#4893=VERTEX_POINT('',#17863);
#4894=VERTEX_POINT('',#17867);
#4895=VERTEX_POINT('',#17869);
#4896=VERTEX_POINT('',#17873);
#4897=VERTEX_POINT('',#17875);
#4898=VERTEX_POINT('',#17879);
#4899=VERTEX_POINT('',#17881);
#4900=VERTEX_POINT('',#17885);
#4901=VERTEX_POINT('',#17887);
#4902=VERTEX_POINT('',#17896);
#4903=VERTEX_POINT('',#17899);
#4904=VERTEX_POINT('',#17902);
#4905=VERTEX_POINT('',#17906);
#4906=VERTEX_POINT('',#17910);
#4907=VERTEX_POINT('',#17914);
#4908=VERTEX_POINT('',#17917);
#5916=EDGE_CURVE('',#4890,#4891,#3546,.T.);
#5917=EDGE_CURVE('',#4891,#4892,#3547,.T.);
#5918=EDGE_CURVE('',#4892,#4893,#3548,.T.);
#5919=EDGE_CURVE('',#4890,#4893,#3549,.T.);
#5920=EDGE_CURVE('',#4891,#4894,#3550,.T.);
#5921=EDGE_CURVE('',#4894,#4895,#3551,.T.);
#5922=EDGE_CURVE('',#4895,#4892,#3552,.T.);
#5923=EDGE_CURVE('',#4894,#4896,#3553,.T.);
#5924=EDGE_CURVE('',#4896,#4897,#3554,.T.);
#5925=EDGE_CURVE('',#4897,#4895,#3555,.T.);
#5926=EDGE_CURVE('',#4896,#4898,#3556,.T.);
#5927=EDGE_CURVE('',#4898,#4899,#3557,.T.);
#5928=EDGE_CURVE('',#4899,#4897,#3558,.T.);
#5929=EDGE_CURVE('',#4898,#4900,#3559,.T.);
#5930=EDGE_CURVE('',#4900,#4901,#3560,.T.);
#5931=EDGE_CURVE('',#4901,#4899,#3561,.T.);
#5932=EDGE_CURVE('',#4900,#4890,#3562,.T.);
#5933=EDGE_CURVE('',#4893,#4901,#3563,.T.);
#5934=EDGE_CURVE('',#4902,#4902,#3011,.T.);
#5935=EDGE_CURVE('',#4903,#4903,#3012,.T.);
#5936=EDGE_CURVE('',#4904,#4904,#3013,.T.);
#5937=EDGE_CURVE('',#4904,#4903,#3564,.T.);
#5938=EDGE_CURVE('',#4905,#4905,#3014,.T.);
#5939=EDGE_CURVE('',#4905,#4904,#3565,.T.);
#5940=EDGE_CURVE('',#4906,#4906,#3015,.T.);
#5941=EDGE_CURVE('',#4906,#4905,#3566,.T.);
#5942=EDGE_CURVE('',#4907,#4907,#3016,.T.);
#5943=EDGE_CURVE('',#4908,#4908,#3017,.F.);
#5944=EDGE_CURVE('',#4908,#4907,#3567,.T.);
#5945=EDGE_CURVE('',#4902,#4908,#3568,.T.);
#7859=ORIENTED_EDGE('',*,*,#5916,.T.);
#7860=ORIENTED_EDGE('',*,*,#5917,.T.);
#7861=ORIENTED_EDGE('',*,*,#5918,.T.);
#7862=ORIENTED_EDGE('',*,*,#5919,.F.);
#7863=ORIENTED_EDGE('',*,*,#5920,.T.);
#7864=ORIENTED_EDGE('',*,*,#5921,.T.);
#7865=ORIENTED_EDGE('',*,*,#5922,.T.);
#7866=ORIENTED_EDGE('',*,*,#5917,.F.);
#7867=ORIENTED_EDGE('',*,*,#5923,.T.);
#7868=ORIENTED_EDGE('',*,*,#5924,.T.);
#7869=ORIENTED_EDGE('',*,*,#5925,.T.);
#7870=ORIENTED_EDGE('',*,*,#5921,.F.);
#7871=ORIENTED_EDGE('',*,*,#5926,.T.);
#7872=ORIENTED_EDGE('',*,*,#5927,.T.);
#7873=ORIENTED_EDGE('',*,*,#5928,.T.);
#7874=ORIENTED_EDGE('',*,*,#5924,.F.);
#7875=ORIENTED_EDGE('',*,*,#5929,.T.);
#7876=ORIENTED_EDGE('',*,*,#5930,.T.);
#7877=ORIENTED_EDGE('',*,*,#5931,.T.);
#7878=ORIENTED_EDGE('',*,*,#5927,.F.);
#7879=ORIENTED_EDGE('',*,*,#5932,.T.);
#7880=ORIENTED_EDGE('',*,*,#5919,.T.);
#7881=ORIENTED_EDGE('',*,*,#5933,.T.);
#7882=ORIENTED_EDGE('',*,*,#5930,.F.);
#7883=ORIENTED_EDGE('',*,*,#5932,.F.);
#7884=ORIENTED_EDGE('',*,*,#5929,.F.);
#7885=ORIENTED_EDGE('',*,*,#5926,.F.);
#7886=ORIENTED_EDGE('',*,*,#5923,.F.);
#7887=ORIENTED_EDGE('',*,*,#5920,.F.);
#7888=ORIENTED_EDGE('',*,*,#5916,.F.);
#7889=ORIENTED_EDGE('',*,*,#5933,.F.);
#7890=ORIENTED_EDGE('',*,*,#5918,.F.);
#7891=ORIENTED_EDGE('',*,*,#5922,.F.);
#7892=ORIENTED_EDGE('',*,*,#5925,.F.);
#7893=ORIENTED_EDGE('',*,*,#5928,.F.);
#7894=ORIENTED_EDGE('',*,*,#5931,.F.);
#7895=ORIENTED_EDGE('',*,*,#5934,.F.);
#7896=ORIENTED_EDGE('',*,*,#5935,.F.);
#7897=ORIENTED_EDGE('',*,*,#5936,.F.);
#7898=ORIENTED_EDGE('',*,*,#5937,.T.);
#7899=ORIENTED_EDGE('',*,*,#5935,.T.);
#7900=ORIENTED_EDGE('',*,*,#5937,.F.);
#7901=ORIENTED_EDGE('',*,*,#5938,.F.);
#7902=ORIENTED_EDGE('',*,*,#5939,.T.);
#7903=ORIENTED_EDGE('',*,*,#5936,.T.);
#7904=ORIENTED_EDGE('',*,*,#5939,.F.);
#7905=ORIENTED_EDGE('',*,*,#5940,.F.);
#7906=ORIENTED_EDGE('',*,*,#5941,.T.);
#7907=ORIENTED_EDGE('',*,*,#5938,.T.);
#7908=ORIENTED_EDGE('',*,*,#5941,.F.);
#7909=ORIENTED_EDGE('',*,*,#5940,.T.);
#7910=ORIENTED_EDGE('',*,*,#5942,.F.);
#7911=ORIENTED_EDGE('',*,*,#5943,.F.);
#7912=ORIENTED_EDGE('',*,*,#5944,.T.);
#7913=ORIENTED_EDGE('',*,*,#5942,.T.);
#7914=ORIENTED_EDGE('',*,*,#5944,.F.);
#7915=ORIENTED_EDGE('',*,*,#5934,.T.);
#7916=ORIENTED_EDGE('',*,*,#5945,.T.);
#7917=ORIENTED_EDGE('',*,*,#5943,.T.);
#7918=ORIENTED_EDGE('',*,*,#5945,.F.);
#8781=PLANE('',#11032);
#8782=PLANE('',#11033);
#8783=PLANE('',#11034);
#8784=PLANE('',#11035);
#8785=PLANE('',#11036);
#8786=PLANE('',#11037);
#8787=PLANE('',#11038);
#8788=PLANE('',#11039);
#8789=PLANE('',#11040);
#8790=PLANE('',#11042);
#8791=PLANE('',#11050);
#9283=ADVANCED_FACE('',(#1678),#8781,.F.);
#9284=ADVANCED_FACE('',(#1679),#8782,.F.);
#9285=ADVANCED_FACE('',(#1680),#8783,.F.);
#9286=ADVANCED_FACE('',(#1681),#8784,.F.);
#9287=ADVANCED_FACE('',(#1682),#8785,.F.);
#9288=ADVANCED_FACE('',(#1683),#8786,.F.);
#9289=ADVANCED_FACE('',(#1684),#8787,.F.);
#9290=ADVANCED_FACE('',(#1685),#8788,.F.);
#9291=ADVANCED_FACE('',(#1686),#8789,.F.);
#9292=ADVANCED_FACE('',(#1687),#8790,.T.);
#9293=ADVANCED_FACE('',(#1688),#541,.T.);
#9294=ADVANCED_FACE('',(#1689),#1232,.T.);
#9295=ADVANCED_FACE('',(#1690),#542,.T.);
#9296=ADVANCED_FACE('',(#1691,#997),#8791,.T.);
#9297=ADVANCED_FACE('',(#1692),#543,.T.);
#9298=ADVANCED_FACE('',(#1693),#1233,.T.);
#9520=CLOSED_SHELL('',(#9283,#9284,#9285,#9286,#9287,#9288,#9289,#9290));
#9521=CLOSED_SHELL('',(#9291,#9292,#9293,#9294,#9295,#9296,#9297,#9298));
#11031=AXIS2_PLACEMENT_3D('',#17856,#13470,#13471);
#11032=AXIS2_PLACEMENT_3D('',#17857,#13472,#13473);
#11033=AXIS2_PLACEMENT_3D('',#17866,#13478,#13479);
#11034=AXIS2_PLACEMENT_3D('',#17872,#13483,#13484);
#11035=AXIS2_PLACEMENT_3D('',#17878,#13488,#13489);
#11036=AXIS2_PLACEMENT_3D('',#17884,#13493,#13494);
#11037=AXIS2_PLACEMENT_3D('',#17890,#13498,#13499);
#11038=AXIS2_PLACEMENT_3D('',#17893,#13502,#13503);
#11039=AXIS2_PLACEMENT_3D('',#17894,#13504,#13505);
#11040=AXIS2_PLACEMENT_3D('',#17895,#13506,#13507);
#11041=AXIS2_PLACEMENT_3D('',#17897,#13508,#13509);
#11042=AXIS2_PLACEMENT_3D('',#17898,#13510,#13511);
#11043=AXIS2_PLACEMENT_3D('',#17900,#13512,#13513);
#11044=AXIS2_PLACEMENT_3D('',#17901,#13514,#13515);
#11045=AXIS2_PLACEMENT_3D('',#17903,#13516,#13517);
#11046=AXIS2_PLACEMENT_3D('',#17905,#13519,#13520);
#11047=AXIS2_PLACEMENT_3D('',#17907,#13521,#13522);
#11048=AXIS2_PLACEMENT_3D('',#17909,#13524,#13525);
#11049=AXIS2_PLACEMENT_3D('',#17911,#13526,#13527);
#11050=AXIS2_PLACEMENT_3D('',#17913,#13529,#13530);
#11051=AXIS2_PLACEMENT_3D('',#17915,#13531,#13532);
#11052=AXIS2_PLACEMENT_3D('',#17916,#13533,#13534);
#11053=AXIS2_PLACEMENT_3D('',#17918,#13535,#13536);
#11054=AXIS2_PLACEMENT_3D('',#17920,#13538,#13539);
#13470=DIRECTION('axis',(0.,0.,1.));
#13471=DIRECTION('refdir',(1.,0.,0.));
#13472=DIRECTION('center_axis',(0.866025403784439,0.,-0.5));
#13473=DIRECTION('ref_axis',(0.5,0.,0.866025403784439));
#13474=DIRECTION('',(-0.5,0.,-0.866025403784439));
#13475=DIRECTION('',(0.,-1.,0.));
#13476=DIRECTION('',(0.5,0.,0.866025403784439));
#13477=DIRECTION('',(0.,-1.,0.));
#13478=DIRECTION('center_axis',(1.60246890531964E-16,0.,-1.));
#13479=DIRECTION('ref_axis',(1.,0.,1.60246890531964E-16));
#13480=DIRECTION('',(-1.,0.,-1.60246890531964E-16));
#13481=DIRECTION('',(0.,-1.,0.));
#13482=DIRECTION('',(1.,0.,1.60246890531964E-16));
#13483=DIRECTION('center_axis',(-0.866025403784439,0.,-0.5));
#13484=DIRECTION('ref_axis',(0.5,0.,-0.866025403784439));
#13485=DIRECTION('',(-0.5,0.,0.866025403784439));
#13486=DIRECTION('',(0.,-1.,0.));
#13487=DIRECTION('',(0.5,0.,-0.866025403784439));
#13488=DIRECTION('center_axis',(-0.866025403784439,0.,0.5));
#13489=DIRECTION('ref_axis',(-0.5,0.,-0.866025403784439));
#13490=DIRECTION('',(0.5,0.,0.866025403784439));
#13491=DIRECTION('',(0.,-1.,0.));
#13492=DIRECTION('',(-0.5,0.,-0.866025403784439));
#13493=DIRECTION('center_axis',(-1.60246890531964E-16,0.,1.));
#13494=DIRECTION('ref_axis',(-1.,0.,-1.60246890531964E-16));
#13495=DIRECTION('',(1.,0.,1.60246890531964E-16));
#13496=DIRECTION('',(0.,-1.,0.));
#13497=DIRECTION('',(-1.,0.,-1.60246890531964E-16));
#13498=DIRECTION('center_axis',(0.866025403784439,0.,0.5));
#13499=DIRECTION('ref_axis',(-0.5,0.,0.866025403784439));
#13500=DIRECTION('',(0.5,0.,-0.866025403784439));
#13501=DIRECTION('',(-0.5,0.,0.866025403784439));
#13502=DIRECTION('center_axis',(0.,1.,0.));
#13503=DIRECTION('ref_axis',(1.,0.,0.));
#13504=DIRECTION('center_axis',(0.,-1.,0.));
#13505=DIRECTION('ref_axis',(0.,0.,-1.));
#13506=DIRECTION('center_axis',(0.,1.,0.));
#13507=DIRECTION('ref_axis',(1.,0.,0.));
#13508=DIRECTION('center_axis',(0.,1.,0.));
#13509=DIRECTION('ref_axis',(1.,0.,0.));
#13510=DIRECTION('center_axis',(0.,1.,0.));
#13511=DIRECTION('ref_axis',(0.,0.,1.));
#13512=DIRECTION('center_axis',(0.,-1.,0.));
#13513=DIRECTION('ref_axis',(1.,0.,0.));
#13514=DIRECTION('center_axis',(0.,-1.,0.));
#13515=DIRECTION('ref_axis',(1.,0.,0.));
#13516=DIRECTION('center_axis',(0.,-1.,0.));
#13517=DIRECTION('ref_axis',(1.,0.,0.));
#13518=DIRECTION('',(0.707106781186547,0.707106781186548,8.65956056235493E-17));
#13519=DIRECTION('center_axis',(0.,-1.,0.));
#13520=DIRECTION('ref_axis',(1.,0.,0.));
#13521=DIRECTION('center_axis',(0.,-1.,0.));
#13522=DIRECTION('ref_axis',(1.,0.,0.));
#13523=DIRECTION('',(0.,1.,0.));
#13524=DIRECTION('center_axis',(0.,1.,0.));
#13525=DIRECTION('ref_axis',(1.,0.,0.));
#13526=DIRECTION('center_axis',(0.,-1.,0.));
#13527=DIRECTION('ref_axis',(1.,0.,0.));
#13528=DIRECTION('',(-0.707106781186547,0.707106781186548,-8.65956056235493E-17));
#13529=DIRECTION('center_axis',(0.,-1.,0.));
#13530=DIRECTION('ref_axis',(0.,0.,-1.));
#13531=DIRECTION('center_axis',(0.,-1.,0.));
#13532=DIRECTION('ref_axis',(1.,0.,0.));
#13533=DIRECTION('center_axis',(0.,1.,0.));
#13534=DIRECTION('ref_axis',(1.,0.,0.));
#13535=DIRECTION('center_axis',(0.,1.,0.));
#13536=DIRECTION('ref_axis',(1.,0.,0.));
#13537=DIRECTION('',(-0.447213595499958,0.894427190999916,-5.47678698264203E-17));
#13538=DIRECTION('center_axis',(0.,-1.,0.));
#13539=DIRECTION('ref_axis',(1.,0.,0.));
#13540=DIRECTION('',(0.,1.,0.));
#17856=CARTESIAN_POINT('',(0.,0.,0.));
#17857=CARTESIAN_POINT('Origin',(0.0866025403784439,-0.4,-0.15));
#17858=CARTESIAN_POINT('',(0.173205080756888,-0.4,0.));
#17859=CARTESIAN_POINT('',(0.0866025403784439,-0.4,-0.15));
#17860=CARTESIAN_POINT('',(0.173205080756888,-0.4,0.));
#17861=CARTESIAN_POINT('',(0.0866025403784439,-0.64,-0.15));
#17862=CARTESIAN_POINT('',(0.0866025403784439,-0.4,-0.15));
#17863=CARTESIAN_POINT('',(0.173205080756888,-0.64,0.));
#17864=CARTESIAN_POINT('',(0.173205080756888,-0.64,0.));
#17865=CARTESIAN_POINT('',(0.173205080756888,-0.4,0.));
#17866=CARTESIAN_POINT('Origin',(-0.0866025403784438,-0.4,-0.15));
#17867=CARTESIAN_POINT('',(-0.0866025403784438,-0.4,-0.15));
#17868=CARTESIAN_POINT('',(0.0866025403784439,-0.4,-0.15));
#17869=CARTESIAN_POINT('',(-0.0866025403784438,-0.64,-0.15));
#17870=CARTESIAN_POINT('',(-0.0866025403784438,-0.4,-0.15));
#17871=CARTESIAN_POINT('',(0.0866025403784439,-0.64,-0.15));
#17872=CARTESIAN_POINT('Origin',(-0.173205080756888,-0.4,-2.77555756156289E-17));
#17873=CARTESIAN_POINT('',(-0.173205080756888,-0.4,-2.12115047744981E-17));
#17874=CARTESIAN_POINT('',(-0.0866025403784438,-0.4,-0.15));
#17875=CARTESIAN_POINT('',(-0.173205080756888,-0.64,-2.77555756156289E-17));
#17876=CARTESIAN_POINT('',(-0.173205080756888,-0.4,-2.12115047744981E-17));
#17877=CARTESIAN_POINT('',(-0.0866025403784438,-0.64,-0.15));
#17878=CARTESIAN_POINT('Origin',(-0.0866025403784439,-0.4,0.15));
#17879=CARTESIAN_POINT('',(-0.0866025403784439,-0.4,0.15));
#17880=CARTESIAN_POINT('',(-0.173205080756888,-0.4,-2.12115047744981E-17));
#17881=CARTESIAN_POINT('',(-0.0866025403784439,-0.64,0.15));
#17882=CARTESIAN_POINT('',(-0.0866025403784439,-0.4,0.15));
#17883=CARTESIAN_POINT('',(-0.173205080756888,-0.64,-2.12115047744981E-17));
#17884=CARTESIAN_POINT('Origin',(0.0866025403784439,-0.4,0.15));
#17885=CARTESIAN_POINT('',(0.0866025403784439,-0.4,0.15));
#17886=CARTESIAN_POINT('',(-0.0866025403784439,-0.4,0.15));
#17887=CARTESIAN_POINT('',(0.0866025403784439,-0.64,0.15));
#17888=CARTESIAN_POINT('',(0.0866025403784439,-0.4,0.15));
#17889=CARTESIAN_POINT('',(-0.0866025403784439,-0.64,0.15));
#17890=CARTESIAN_POINT('Origin',(0.173205080756888,-0.4,0.));
#17891=CARTESIAN_POINT('',(0.0866025403784439,-0.4,0.15));
#17892=CARTESIAN_POINT('',(0.0866025403784439,-0.64,0.15));
#17893=CARTESIAN_POINT('Origin',(0.,-0.4,-2.77555756156289E-17));
#17894=CARTESIAN_POINT('Origin',(0.,-0.64,-2.77555756156289E-17));
#17895=CARTESIAN_POINT('Origin',(0.,-1.4,0.));
#17896=CARTESIAN_POINT('',(-0.1954,-1.4,2.39295984553393E-17));
#17897=CARTESIAN_POINT('Origin',(0.,-1.4,0.));
#17898=CARTESIAN_POINT('Origin',(0.3,0.4,0.));
#17899=CARTESIAN_POINT('',(-0.3,0.4,-3.67394039744206E-17));
#17900=CARTESIAN_POINT('Origin',(0.,0.4,0.));
#17901=CARTESIAN_POINT('Origin',(0.,0.375,0.));
#17902=CARTESIAN_POINT('',(-0.35,0.35,-4.28626379701573E-17));
#17903=CARTESIAN_POINT('Origin',(0.,0.35,0.));
#17904=CARTESIAN_POINT('',(-0.325,0.375,-3.9801020972289E-17));
#17905=CARTESIAN_POINT('Origin',(0.,0.19,0.));
#17906=CARTESIAN_POINT('',(-0.35,0.03,-4.28626379701574E-17));
#17907=CARTESIAN_POINT('Origin',(0.,0.03,0.));
#17908=CARTESIAN_POINT('',(-0.35,0.19,-4.28626379701574E-17));
#17909=CARTESIAN_POINT('Origin',(0.,0.0149999999999999,0.));
#17910=CARTESIAN_POINT('',(-0.32,-3.29597460435593E-17,-3.91886975727153E-17));
#17911=CARTESIAN_POINT('Origin',(0.,0.,0.));
#17912=CARTESIAN_POINT('',(-0.335,0.0149999999999999,-4.10256677714363E-17));
#17913=CARTESIAN_POINT('Origin',(0.22,0.,0.));
#17914=CARTESIAN_POINT('',(-0.22,-6.93889390390723E-18,-2.69422295812418E-17));
#17915=CARTESIAN_POINT('Origin',(0.,0.,0.));
#17916=CARTESIAN_POINT('Origin',(0.,-0.02,0.));
#17917=CARTESIAN_POINT('',(-0.1954,-0.0492,2.39295984553393E-17));
#17918=CARTESIAN_POINT('Origin',(0.,-0.0492,0.));
#17919=CARTESIAN_POINT('',(-0.21,-0.02,-2.57175827820944E-17));
#17920=CARTESIAN_POINT('Origin',(0.,-0.8,0.));
#17921=CARTESIAN_POINT('',(-0.1954,-0.8,-2.39295984553393E-17));
#18944=UNCERTAINTY_MEASURE_WITH_UNIT(LENGTH_MEASURE(0.001),#19044,
'DISTANCE_ACCURACY_VALUE',
'Maximum model space distance between geometric entities at asserted c
onnectivities');
#18972=UNCERTAINTY_MEASURE_WITH_UNIT(LENGTH_MEASURE(0.001),#19044,
'DISTANCE_ACCURACY_VALUE',
'Maximum model space distance between geometric entities at asserted c
onnectivities');
#19015=(
GEOMETRIC_REPRESENTATION_CONTEXT(3)
GLOBAL_UNCERTAINTY_ASSIGNED_CONTEXT((#18944))
GLOBAL_UNIT_ASSIGNED_CONTEXT((#19044,#19046,#19047))
REPRESENTATION_CONTEXT('','3D')
);
#19043=(
GEOMETRIC_REPRESENTATION_CONTEXT(3)
GLOBAL_UNCERTAINTY_ASSIGNED_CONTEXT((#18972))
GLOBAL_UNIT_ASSIGNED_CONTEXT((#19044,#19046,#19047))
REPRESENTATION_CONTEXT('','3D')
);
#19044=(
LENGTH_UNIT()
NAMED_UNIT(*)
SI_UNIT(.CENTI.,.METRE.)
);
#19046=(
NAMED_UNIT(*)
PLANE_ANGLE_UNIT()
SI_UNIT($,.RADIAN.)
);
#19047=(
NAMED_UNIT(*)
SI_UNIT($,.STERADIAN.)
SOLID_ANGLE_UNIT()
);
#19090=SHAPE_DEFINITION_REPRESENTATION(#19167,#19348);
#19167=PRODUCT_DEFINITION_SHAPE('',$,#19419);
#19348=SHAPE_REPRESENTATION('',(#11031),#19015);
#19376=PRODUCT_DEFINITION_CONTEXT('part definition',#19588,'design');
#19419=PRODUCT_DEFINITION('2026-11-03-00-38-46-506',
'M4x14 manifold screw',#19489,#19376);
#19489=PRODUCT_DEFINITION_FORMATION('',$,#19632);
#19588=APPLICATION_CONTEXT(
'Core Data for Automotive Mechanical Design Process');
#19589=PRODUCT_CONTEXT('part definition',#19588,'mechanical');
#19632=PRODUCT('2026-11-03-00-38-46-506','M4x14 manifold screw',
'M4x14 manifold screw',(#19589));
#19663=PRESENTATION_STYLE_ASSIGNMENT((#19669));
#19669=SURFACE_STYLE_USAGE(.BOTH.,#19675);
#19675=SURFACE_SIDE_STYLE('',(#19681));
#19681=SURFACE_STYLE_FILL_AREA(#19687);
#19687=FILL_AREA_STYLE('CAD Library Painted - Graphite',(#19693));
#19693=FILL_AREA_STYLE_COLOUR('CAD Library Painted - Graphite',#19699);
#19699=COLOUR_RGB('CAD Library Painted - Graphite',0.168627450980392,0.192156862745098,
0.231372549019608);
ENDSEC;
END-ISO-10303-21;
